ISO-10303-21;
HEADER;
/* Generated by software containing ST-Developer
 * from STEP Tools, Inc. (www.steptools.com) 
 */

FILE_DESCRIPTION(
/* description */ ('STEP AP214'),
/* implementation_level */ '2;1');

FILE_NAME(
/* name */ 'Narrow Flat Washer 0.625.step',
/* time_stamp */ '2026-11-14T07:13:32-08:00',
/* author */ (''),
/* organization */ (''),
/* preprocessor_version */ 'ST-DEVELOPER v20.2',
/* originating_system */ 'Autodesk Translation Framework v15.17.0.0',
/* authorisation */ '');

FILE_SCHEMA (('AUTOMOTIVE_DESIGN { 1 0 10303 214 3 1 1 }'));
ENDSEC;

DATA;
#10=MECHANICAL_DESIGN_GEOMETRIC_PRESENTATION_REPRESENTATION('',(#1324),#32903);
#681=SHAPE_REPRESENTATION_RELATIONSHIP('SRR','None',#33023,#695);
#695=ADVANCED_BREP_SHAPE_REPRESENTATION('',(#1413),#32898);
#965=CIRCLE('',#16521,16.6624);
#966=CIRCLE('',#16522,16.6624);
#967=CIRCLE('',#16524,8.3312);
#968=CIRCLE('',#16525,8.3312);
#1248=CYLINDRICAL_SURFACE('',#16520,16.6624);
#1249=CYLINDRICAL_SURFACE('',#16523,8.3312);
#1324=STYLED_ITEM('',(#33099),#1413);
#1413=MANIFOLD_SOLID_BREP('Body1',#15572);
#1603=FACE_BOUND('',#3158,.T.);
#1604=FACE_BOUND('',#3160,.T.);
#2126=FACE_OUTER_BOUND('',#3155,.T.);
#2127=FACE_OUTER_BOUND('',#3156,.T.);
#2128=FACE_OUTER_BOUND('',#3157,.T.);
#2129=FACE_OUTER_BOUND('',#3159,.T.);
#3155=EDGE_LOOP('',(#12109,#12110,#12111,#12112));
#3156=EDGE_LOOP('',(#12113,#12114,#12115,#12116));
#3157=EDGE_LOOP('',(#12117));
#3158=EDGE_LOOP('',(#12118));
#3159=EDGE_LOOP('',(#12119));
#3160=EDGE_LOOP('',(#12120));
#4260=LINE('',#30675,#5664);
#4261=LINE('',#30681,#5665);
#5664=VECTOR('',#19222,16.6624);
#5665=VECTOR('',#19229,8.3312);
#7200=VERTEX_POINT('',#30672);
#7201=VERTEX_POINT('',#30674);
#7202=VERTEX_POINT('',#30678);
#7203=VERTEX_POINT('',#30680);
#8938=EDGE_CURVE('',#7200,#7200,#965,.T.);
#8939=EDGE_CURVE('',#7200,#7201,#4260,.T.);
#8940=EDGE_CURVE('',#7201,#7201,#966,.T.);
#8941=EDGE_CURVE('',#7202,#7202,#967,.T.);
#8942=EDGE_CURVE('',#7202,#7203,#4261,.T.);
#8943=EDGE_CURVE('',#7203,#7203,#968,.T.);
#12109=ORIENTED_EDGE('',*,*,#8938,.F.);
#12110=ORIENTED_EDGE('',*,*,#8939,.T.);
#12111=ORIENTED_EDGE('',*,*,#8940,.T.);
#12112=ORIENTED_EDGE('',*,*,#8939,.F.);
#12113=ORIENTED_EDGE('',*,*,#8941,.F.);
#12114=ORIENTED_EDGE('',*,*,#8942,.T.);
#12115=ORIENTED_EDGE('',*,*,#8943,.T.);
#12116=ORIENTED_EDGE('',*,*,#8942,.F.);
#12117=ORIENTED_EDGE('',*,*,#8940,.F.);
#12118=ORIENTED_EDGE('',*,*,#8941,.T.);
#12119=ORIENTED_EDGE('',*,*,#8938,.T.);
#12120=ORIENTED_EDGE('',*,*,#8943,.F.);
#14264=PLANE('',#16526);
#14265=PLANE('',#16527);
#15094=ADVANCED_FACE('',(#2126),#1248,.T.);
#15095=ADVANCED_FACE('',(#2127),#1249,.F.);
#15096=ADVANCED_FACE('',(#2128,#1603),#14264,.F.);
#15097=ADVANCED_FACE('',(#2129,#1604),#14265,.F.);
#15572=CLOSED_SHELL('',(#15094,#15095,#15096,#15097));
#16519=AXIS2_PLACEMENT_3D('',#30670,#19216,#19217);
#16520=AXIS2_PLACEMENT_3D('',#30671,#19218,#19219);
#16521=AXIS2_PLACEMENT_3D('',#30673,#19220,#19221);
#16522=AXIS2_PLACEMENT_3D('',#30676,#19223,#19224);
#16523=AXIS2_PLACEMENT_3D('',#30677,#19225,#19226);
#16524=AXIS2_PLACEMENT_3D('',#30679,#19227,#19228);
#16525=AXIS2_PLACEMENT_3D('',#30682,#19230,#19231);
#16526=AXIS2_PLACEMENT_3D('',#30683,#19232,#19233);
#16527=AXIS2_PLACEMENT_3D('',#30684,#19234,#19235);
#19216=DIRECTION('axis',(0.,0.,1.));
#19217=DIRECTION('refdir',(1.,0.,0.));
#19218=DIRECTION('center_axis',(-1.,0.,0.));
#19219=DIRECTION('ref_axis',(0.,0.,1.));
#19220=DIRECTION('center_axis',(-1.,0.,0.));
#19221=DIRECTION('ref_axis',(0.,0.,1.));
#19222=DIRECTION('',(1.,0.,0.));
#19223=DIRECTION('center_axis',(-1.,0.,0.));
#19224=DIRECTION('ref_axis',(0.,0.,1.));
#19225=DIRECTION('center_axis',(-1.,0.,0.));
#19226=DIRECTION('ref_axis',(0.,0.,1.));
#19227=DIRECTION('center_axis',(-1.,0.,0.));
#19228=DIRECTION('ref_axis',(0.,0.,1.));
#19229=DIRECTION('',(-1.,0.,0.));
#19230=DIRECTION('center_axis',(-1.,0.,0.));
#19231=DIRECTION('ref_axis',(0.,0.,1.));
#19232=DIRECTION('center_axis',(-1.,0.,0.));
#19233=DIRECTION('ref_axis',(0.,0.,1.));
#19234=DIRECTION('center_axis',(1.,0.,0.));
#19235=DIRECTION('ref_axis',(0.,0.,-1.));
#30670=CARTESIAN_POINT('',(0.,0.,0.));
#30671=CARTESIAN_POINT('Origin',(-34.9249999999999,0.,0.));
#30672=CARTESIAN_POINT('',(-2.413,-2.04055548261129E-15,-16.6624));
#30673=CARTESIAN_POINT('Origin',(-2.413,0.,0.));
#30674=CARTESIAN_POINT('',(0.,-2.04055548261129E-15,-16.6624));
#30675=CARTESIAN_POINT('',(-34.9249999999999,-2.04055548261129E-15,-16.6624));
#30676=CARTESIAN_POINT('Origin',(0.,0.,0.));
#30677=CARTESIAN_POINT('Origin',(-34.9249999999999,0.,0.));
#30678=CARTESIAN_POINT('',(0.,-1.02027774130564E-15,-8.3312));
#30679=CARTESIAN_POINT('Origin',(0.,0.,0.));
#30680=CARTESIAN_POINT('',(-2.413,-1.02027774130564E-15,-8.3312));
#30681=CARTESIAN_POINT('',(-34.9249999999999,-1.02027774130564E-15,-8.3312));
#30682=CARTESIAN_POINT('Origin',(-2.413,0.,0.));
#30683=CARTESIAN_POINT('Origin',(0.,8.3312,0.));
#30684=CARTESIAN_POINT('Origin',(-2.413,16.6624,0.));
#32881=UNCERTAINTY_MEASURE_WITH_UNIT(LENGTH_MEASURE(0.01),#32904,
'DISTANCE_ACCURACY_VALUE',
'Maximum model space distance between geometric entities at asserted c
onnectivities');
#32886=UNCERTAINTY_MEASURE_WITH_UNIT(LENGTH_MEASURE(0.01),#32904,
'DISTANCE_ACCURACY_VALUE',
'Maximum model space distance between geometric entities at asserted c
onnectivities');
#32898=(
GEOMETRIC_REPRESENTATION_CONTEXT(3)
GLOBAL_UNCERTAINTY_ASSIGNED_CONTEXT((#32881))
GLOBAL_UNIT_ASSIGNED_CONTEXT((#32904,#32906,#32907))
REPRESENTATION_CONTEXT('','3D')
);
#32903=(
GEOMETRIC_REPRESENTATION_CONTEXT(3)
GLOBAL_UNCERTAINTY_ASSIGNED_CONTEXT((#32886))
GLOBAL_UNIT_ASSIGNED_CONTEXT((#32904,#32906,#32907))
REPRESENTATION_CONTEXT('','3D')
);
#32904=(
LENGTH_UNIT()
NAMED_UNIT(*)
SI_UNIT(.MILLI.,.METRE.)
);
#32906=(
NAMED_UNIT(*)
PLANE_ANGLE_UNIT()
SI_UNIT($,.RADIAN.)
);
#32907=(
NAMED_UNIT(*)
SI_UNIT($,.STERADIAN.)
SOLID_ANGLE_UNIT()
);
#32919=SHAPE_DEFINITION_REPRESENTATION(#32935,#33023);
#32935=PRODUCT_DEFINITION_SHAPE('',$,#33040);
#33023=SHAPE_REPRESENTATION('',(#16519),#32898);
#33028=PRODUCT_DEFINITION_CONTEXT('part definition',#33078,'design');
#33040=PRODUCT_DEFINITION('Narrow Flat Washer 0.625',
'Narrow Flat Washer 0.625',#33056,#33028);
#33056=PRODUCT_DEFINITION_FORMATION('',$,#33091);
#33078=APPLICATION_CONTEXT(
'Core Data for Automotive Mechanical Design Process');
#33079=PRODUCT_CONTEXT('part definition',#33078,'mechanical');
#33091=PRODUCT('Narrow Flat Washer 0.625','Narrow Flat Washer 0.625',$,
(#33079));
#33099=PRESENTATION_STYLE_ASSIGNMENT((#33105));
#33105=SURFACE_STYLE_USAGE(.BOTH.,#33111);
#33111=SURFACE_SIDE_STYLE('',(#33117));
#33117=SURFACE_STYLE_FILL_AREA(#33123);
#33123=FILL_AREA_STYLE('Opaque(31,36,43)',(#33129));
#33129=FILL_AREA_STYLE_COLOUR('Opaque(31,36,43)',#33135);
#33135=COLOUR_RGB('Opaque(31,36,43)',0.12156862745098,0.141176470588235,
0.168627450980392);
ENDSEC;
END-ISO-10303-21;
